ISO-10303-21;
HEADER;
/* Generated by software containing ST-Developer
 * from STEP Tools, Inc. (www.steptools.com) 
 */

FILE_DESCRIPTION(
/* description */ ('Twin-shaft manual slide'),
/* implementation_level */ '2;1');

FILE_NAME(
/* name */ 'Cap Screw - M6x25.step',
/* time_stamp */ '2026-10-27T18:38:08-07:00',
/* author */ (''),
/* organization */ (''),
/* preprocessor_version */ 'ST-DEVELOPER v20.2',
/* originating_system */ 'Autodesk Translation Framework v15.17.0.0',
/* authorisation */ '');

FILE_SCHEMA (('AUTOMOTIVE_DESIGN { 1 0 10303 214 3 1 1 }'));
ENDSEC;

DATA;
#10=MECHANICAL_DESIGN_GEOMETRIC_PRESENTATION_REPRESENTATION('',(#291),#6463);
#222=ORIENTED_CLOSED_SHELL('',*,#3657,.F.);
#226=BREP_WITH_VOIDS('Body1',#3656,(#222));
#240=CONICAL_SURFACE('',#4221,0.475,0.785398163397449);
#241=CONICAL_SURFACE('',#4225,0.485,0.785398163397448);
#242=CONICAL_SURFACE('',#4229,0.31,0.463647609000806);
#243=CONICAL_SURFACE('',#4233,0.27,0.785398163397448);
#259=SHAPE_REPRESENTATION_RELATIONSHIP('SRR','None',#6579,#275);
#275=ADVANCED_BREP_SHAPE_REPRESENTATION('',(#226),#6462);
#291=STYLED_ITEM('',(#6747),#226);
#400=FACE_BOUND('',#1024,.T.);
#515=PLANE('',#4219);
#516=PLANE('',#4227);
#517=PLANE('',#4235);
#518=PLANE('',#4236);
#519=PLANE('',#4237);
#520=PLANE('',#4238);
#521=PLANE('',#4239);
#522=PLANE('',#4240);
#523=PLANE('',#4241);
#524=PLANE('',#4242);
#525=PLANE('',#4243);
#716=FACE_OUTER_BOUND('',#1019,.T.);
#717=FACE_OUTER_BOUND('',#1020,.T.);
#718=FACE_OUTER_BOUND('',#1021,.T.);
#719=FACE_OUTER_BOUND('',#1022,.T.);
#720=FACE_OUTER_BOUND('',#1023,.T.);
#721=FACE_OUTER_BOUND('',#1025,.T.);
#722=FACE_OUTER_BOUND('',#1026,.T.);
#723=FACE_OUTER_BOUND('',#1027,.T.);
#724=FACE_OUTER_BOUND('',#1028,.T.);
#725=FACE_OUTER_BOUND('',#1029,.T.);
#726=FACE_OUTER_BOUND('',#1030,.T.);
#727=FACE_OUTER_BOUND('',#1031,.T.);
#728=FACE_OUTER_BOUND('',#1032,.T.);
#729=FACE_OUTER_BOUND('',#1033,.T.);
#730=FACE_OUTER_BOUND('',#1034,.T.);
#731=FACE_OUTER_BOUND('',#1035,.T.);
#732=FACE_OUTER_BOUND('',#1036,.T.);
#1019=EDGE_LOOP('',(#3302));
#1020=EDGE_LOOP('',(#3303,#3304,#3305,#3306));
#1021=EDGE_LOOP('',(#3307,#3308,#3309,#3310));
#1022=EDGE_LOOP('',(#3311,#3312,#3313,#3314));
#1023=EDGE_LOOP('',(#3315));
#1024=EDGE_LOOP('',(#3316));
#1025=EDGE_LOOP('',(#3317,#3318,#3319,#3320));
#1026=EDGE_LOOP('',(#3321,#3322,#3323,#3324));
#1027=EDGE_LOOP('',(#3325,#3326,#3327,#3328));
#1028=EDGE_LOOP('',(#3329));
#1029=EDGE_LOOP('',(#3330,#3331,#3332,#3333));
#1030=EDGE_LOOP('',(#3334,#3335,#3336,#3337));
#1031=EDGE_LOOP('',(#3338,#3339,#3340,#3341));
#1032=EDGE_LOOP('',(#3342,#3343,#3344,#3345));
#1033=EDGE_LOOP('',(#3346,#3347,#3348,#3349));
#1034=EDGE_LOOP('',(#3350,#3351,#3352,#3353));
#1035=EDGE_LOOP('',(#3354,#3355,#3356,#3357,#3358,#3359));
#1036=EDGE_LOOP('',(#3360,#3361,#3362,#3363,#3364,#3365));
#1299=LINE('',#6336,#1585);
#1300=LINE('',#6340,#1586);
#1301=LINE('',#6344,#1587);
#1302=LINE('',#6351,#1588);
#1303=LINE('',#6355,#1589);
#1304=LINE('',#6359,#1590);
#1305=LINE('',#6364,#1591);
#1306=LINE('',#6366,#1592);
#1307=LINE('',#6368,#1593);
#1308=LINE('',#6369,#1594);
#1309=LINE('',#6372,#1595);
#1310=LINE('',#6374,#1596);
#1311=LINE('',#6375,#1597);
#1312=LINE('',#6378,#1598);
#1313=LINE('',#6380,#1599);
#1314=LINE('',#6381,#1600);
#1315=LINE('',#6384,#1601);
#1316=LINE('',#6386,#1602);
#1317=LINE('',#6387,#1603);
#1318=LINE('',#6390,#1604);
#1319=LINE('',#6392,#1605);
#1320=LINE('',#6393,#1606);
#1321=LINE('',#6395,#1607);
#1322=LINE('',#6396,#1608);
#1585=VECTOR('',#5305,0.475);
#1586=VECTOR('',#5310,0.5);
#1587=VECTOR('',#5315,0.485);
#1588=VECTOR('',#5324,0.31);
#1589=VECTOR('',#5329,0.3);
#1590=VECTOR('',#5334,0.27);
#1591=VECTOR('',#5339,1.);
#1592=VECTOR('',#5340,1.);
#1593=VECTOR('',#5341,1.);
#1594=VECTOR('',#5342,1.);
#1595=VECTOR('',#5345,1.);
#1596=VECTOR('',#5346,1.);
#1597=VECTOR('',#5347,1.);
#1598=VECTOR('',#5350,1.);
#1599=VECTOR('',#5351,1.);
#1600=VECTOR('',#5352,1.);
#1601=VECTOR('',#5355,1.);
#1602=VECTOR('',#5356,1.);
#1603=VECTOR('',#5357,1.);
#1604=VECTOR('',#5360,1.);
#1605=VECTOR('',#5361,1.);
#1606=VECTOR('',#5362,1.);
#1607=VECTOR('',#5365,1.);
#1608=VECTOR('',#5366,1.);
#1754=CIRCLE('',#4220,0.45);
#1755=CIRCLE('',#4222,0.5);
#1756=CIRCLE('',#4224,0.5);
#1757=CIRCLE('',#4226,0.47);
#1758=CIRCLE('',#4228,0.32);
#1759=CIRCLE('',#4230,0.2942);
#1760=CIRCLE('',#4232,0.2942);
#1761=CIRCLE('',#4234,0.24);
#2029=VERTEX_POINT('',#6331);
#2030=VERTEX_POINT('',#6334);
#2031=VERTEX_POINT('',#6338);
#2032=VERTEX_POINT('',#6342);
#2033=VERTEX_POINT('',#6346);
#2034=VERTEX_POINT('',#6349);
#2035=VERTEX_POINT('',#6353);
#2036=VERTEX_POINT('',#6357);
#2037=VERTEX_POINT('',#6362);
#2038=VERTEX_POINT('',#6363);
#2039=VERTEX_POINT('',#6365);
#2040=VERTEX_POINT('',#6367);
#2041=VERTEX_POINT('',#6371);
#2042=VERTEX_POINT('',#6373);
#2043=VERTEX_POINT('',#6377);
#2044=VERTEX_POINT('',#6379);
#2045=VERTEX_POINT('',#6383);
#2046=VERTEX_POINT('',#6385);
#2047=VERTEX_POINT('',#6389);
#2048=VERTEX_POINT('',#6391);
#2456=EDGE_CURVE('',#2029,#2029,#1754,.T.);
#2457=EDGE_CURVE('',#2030,#2030,#1755,.T.);
#2458=EDGE_CURVE('',#2030,#2029,#1299,.T.);
#2459=EDGE_CURVE('',#2031,#2031,#1756,.T.);
#2460=EDGE_CURVE('',#2031,#2030,#1300,.T.);
#2461=EDGE_CURVE('',#2032,#2032,#1757,.T.);
#2462=EDGE_CURVE('',#2032,#2031,#1301,.T.);
#2463=EDGE_CURVE('',#2033,#2033,#1758,.T.);
#2464=EDGE_CURVE('',#2034,#2034,#1759,.F.);
#2465=EDGE_CURVE('',#2034,#2033,#1302,.T.);
#2466=EDGE_CURVE('',#2035,#2035,#1760,.F.);
#2467=EDGE_CURVE('',#2035,#2034,#1303,.T.);
#2468=EDGE_CURVE('',#2036,#2036,#1761,.T.);
#2469=EDGE_CURVE('',#2036,#2035,#1304,.T.);
#2470=EDGE_CURVE('',#2037,#2038,#1305,.T.);
#2471=EDGE_CURVE('',#2038,#2039,#1306,.T.);
#2472=EDGE_CURVE('',#2039,#2040,#1307,.T.);
#2473=EDGE_CURVE('',#2037,#2040,#1308,.T.);
#2474=EDGE_CURVE('',#2038,#2041,#1309,.T.);
#2475=EDGE_CURVE('',#2041,#2042,#1310,.T.);
#2476=EDGE_CURVE('',#2042,#2039,#1311,.T.);
#2477=EDGE_CURVE('',#2041,#2043,#1312,.T.);
#2478=EDGE_CURVE('',#2043,#2044,#1313,.T.);
#2479=EDGE_CURVE('',#2044,#2042,#1314,.T.);
#2480=EDGE_CURVE('',#2043,#2045,#1315,.T.);
#2481=EDGE_CURVE('',#2045,#2046,#1316,.T.);
#2482=EDGE_CURVE('',#2046,#2044,#1317,.T.);
#2483=EDGE_CURVE('',#2045,#2047,#1318,.T.);
#2484=EDGE_CURVE('',#2047,#2048,#1319,.T.);
#2485=EDGE_CURVE('',#2048,#2046,#1320,.T.);
#2486=EDGE_CURVE('',#2047,#2037,#1321,.T.);
#2487=EDGE_CURVE('',#2040,#2048,#1322,.T.);
#3302=ORIENTED_EDGE('',*,*,#2456,.F.);
#3303=ORIENTED_EDGE('',*,*,#2457,.F.);
#3304=ORIENTED_EDGE('',*,*,#2458,.T.);
#3305=ORIENTED_EDGE('',*,*,#2456,.T.);
#3306=ORIENTED_EDGE('',*,*,#2458,.F.);
#3307=ORIENTED_EDGE('',*,*,#2459,.F.);
#3308=ORIENTED_EDGE('',*,*,#2460,.T.);
#3309=ORIENTED_EDGE('',*,*,#2457,.T.);
#3310=ORIENTED_EDGE('',*,*,#2460,.F.);
#3311=ORIENTED_EDGE('',*,*,#2461,.F.);
#3312=ORIENTED_EDGE('',*,*,#2462,.T.);
#3313=ORIENTED_EDGE('',*,*,#2459,.T.);
#3314=ORIENTED_EDGE('',*,*,#2462,.F.);
#3315=ORIENTED_EDGE('',*,*,#2461,.T.);
#3316=ORIENTED_EDGE('',*,*,#2463,.F.);
#3317=ORIENTED_EDGE('',*,*,#2464,.F.);
#3318=ORIENTED_EDGE('',*,*,#2465,.T.);
#3319=ORIENTED_EDGE('',*,*,#2463,.T.);
#3320=ORIENTED_EDGE('',*,*,#2465,.F.);
#3321=ORIENTED_EDGE('',*,*,#2466,.F.);
#3322=ORIENTED_EDGE('',*,*,#2467,.T.);
#3323=ORIENTED_EDGE('',*,*,#2464,.T.);
#3324=ORIENTED_EDGE('',*,*,#2467,.F.);
#3325=ORIENTED_EDGE('',*,*,#2468,.F.);
#3326=ORIENTED_EDGE('',*,*,#2469,.T.);
#3327=ORIENTED_EDGE('',*,*,#2466,.T.);
#3328=ORIENTED_EDGE('',*,*,#2469,.F.);
#3329=ORIENTED_EDGE('',*,*,#2468,.T.);
#3330=ORIENTED_EDGE('',*,*,#2470,.T.);
#3331=ORIENTED_EDGE('',*,*,#2471,.T.);
#3332=ORIENTED_EDGE('',*,*,#2472,.T.);
#3333=ORIENTED_EDGE('',*,*,#2473,.F.);
#3334=ORIENTED_EDGE('',*,*,#2474,.T.);
#3335=ORIENTED_EDGE('',*,*,#2475,.T.);
#3336=ORIENTED_EDGE('',*,*,#2476,.T.);
#3337=ORIENTED_EDGE('',*,*,#2471,.F.);
#3338=ORIENTED_EDGE('',*,*,#2477,.T.);
#3339=ORIENTED_EDGE('',*,*,#2478,.T.);
#3340=ORIENTED_EDGE('',*,*,#2479,.T.);
#3341=ORIENTED_EDGE('',*,*,#2475,.F.);
#3342=ORIENTED_EDGE('',*,*,#2480,.T.);
#3343=ORIENTED_EDGE('',*,*,#2481,.T.);
#3344=ORIENTED_EDGE('',*,*,#2482,.T.);
#3345=ORIENTED_EDGE('',*,*,#2478,.F.);
#3346=ORIENTED_EDGE('',*,*,#2483,.T.);
#3347=ORIENTED_EDGE('',*,*,#2484,.T.);
#3348=ORIENTED_EDGE('',*,*,#2485,.T.);
#3349=ORIENTED_EDGE('',*,*,#2481,.F.);
#3350=ORIENTED_EDGE('',*,*,#2486,.T.);
#3351=ORIENTED_EDGE('',*,*,#2473,.T.);
#3352=ORIENTED_EDGE('',*,*,#2487,.T.);
#3353=ORIENTED_EDGE('',*,*,#2484,.F.);
#3354=ORIENTED_EDGE('',*,*,#2486,.F.);
#3355=ORIENTED_EDGE('',*,*,#2483,.F.);
#3356=ORIENTED_EDGE('',*,*,#2480,.F.);
#3357=ORIENTED_EDGE('',*,*,#2477,.F.);
#3358=ORIENTED_EDGE('',*,*,#2474,.F.);
#3359=ORIENTED_EDGE('',*,*,#2470,.F.);
#3360=ORIENTED_EDGE('',*,*,#2487,.F.);
#3361=ORIENTED_EDGE('',*,*,#2472,.F.);
#3362=ORIENTED_EDGE('',*,*,#2476,.F.);
#3363=ORIENTED_EDGE('',*,*,#2479,.F.);
#3364=ORIENTED_EDGE('',*,*,#2482,.F.);
#3365=ORIENTED_EDGE('',*,*,#2485,.F.);
#3429=CYLINDRICAL_SURFACE('',#4223,0.5);
#3430=CYLINDRICAL_SURFACE('',#4231,0.2942);
#3621=ADVANCED_FACE('',(#716),#515,.T.);
#3622=ADVANCED_FACE('',(#717),#240,.T.);
#3623=ADVANCED_FACE('',(#718),#3429,.T.);
#3624=ADVANCED_FACE('',(#719),#241,.T.);
#3625=ADVANCED_FACE('',(#720,#400),#516,.T.);
#3626=ADVANCED_FACE('',(#721),#242,.T.);
#3627=ADVANCED_FACE('',(#722),#3430,.T.);
#3628=ADVANCED_FACE('',(#723),#243,.T.);
#3629=ADVANCED_FACE('',(#724),#517,.T.);
#3630=ADVANCED_FACE('',(#725),#518,.F.);
#3631=ADVANCED_FACE('',(#726),#519,.F.);
#3632=ADVANCED_FACE('',(#727),#520,.F.);
#3633=ADVANCED_FACE('',(#728),#521,.F.);
#3634=ADVANCED_FACE('',(#729),#522,.F.);
#3635=ADVANCED_FACE('',(#730),#523,.F.);
#3636=ADVANCED_FACE('',(#731),#524,.F.);
#3637=ADVANCED_FACE('',(#732),#525,.F.);
#3656=CLOSED_SHELL('',(#3621,#3622,#3623,#3624,#3625,#3626,#3627,#3628,
#3629));
#3657=CLOSED_SHELL('',(#3630,#3631,#3632,#3633,#3634,#3635,#3636,#3637));
#4218=AXIS2_PLACEMENT_3D('',#6329,#5295,#5296);
#4219=AXIS2_PLACEMENT_3D('',#6330,#5297,#5298);
#4220=AXIS2_PLACEMENT_3D('',#6332,#5299,#5300);
#4221=AXIS2_PLACEMENT_3D('',#6333,#5301,#5302);
#4222=AXIS2_PLACEMENT_3D('',#6335,#5303,#5304);
#4223=AXIS2_PLACEMENT_3D('',#6337,#5306,#5307);
#4224=AXIS2_PLACEMENT_3D('',#6339,#5308,#5309);
#4225=AXIS2_PLACEMENT_3D('',#6341,#5311,#5312);
#4226=AXIS2_PLACEMENT_3D('',#6343,#5313,#5314);
#4227=AXIS2_PLACEMENT_3D('',#6345,#5316,#5317);
#4228=AXIS2_PLACEMENT_3D('',#6347,#5318,#5319);
#4229=AXIS2_PLACEMENT_3D('',#6348,#5320,#5321);
#4230=AXIS2_PLACEMENT_3D('',#6350,#5322,#5323);
#4231=AXIS2_PLACEMENT_3D('',#6352,#5325,#5326);
#4232=AXIS2_PLACEMENT_3D('',#6354,#5327,#5328);
#4233=AXIS2_PLACEMENT_3D('',#6356,#5330,#5331);
#4234=AXIS2_PLACEMENT_3D('',#6358,#5332,#5333);
#4235=AXIS2_PLACEMENT_3D('',#6360,#5335,#5336);
#4236=AXIS2_PLACEMENT_3D('',#6361,#5337,#5338);
#4237=AXIS2_PLACEMENT_3D('',#6370,#5343,#5344);
#4238=AXIS2_PLACEMENT_3D('',#6376,#5348,#5349);
#4239=AXIS2_PLACEMENT_3D('',#6382,#5353,#5354);
#4240=AXIS2_PLACEMENT_3D('',#6388,#5358,#5359);
#4241=AXIS2_PLACEMENT_3D('',#6394,#5363,#5364);
#4242=AXIS2_PLACEMENT_3D('',#6397,#5367,#5368);
#4243=AXIS2_PLACEMENT_3D('',#6398,#5369,#5370);
#5295=DIRECTION('axis',(0.,0.,1.));
#5296=DIRECTION('refdir',(1.,0.,0.));
#5297=DIRECTION('center_axis',(0.,1.,0.));
#5298=DIRECTION('ref_axis',(0.,0.,1.));
#5299=DIRECTION('center_axis',(0.,-1.,0.));
#5300=DIRECTION('ref_axis',(1.,0.,0.));
#5301=DIRECTION('center_axis',(0.,-1.,0.));
#5302=DIRECTION('ref_axis',(1.,0.,0.));
#5303=DIRECTION('center_axis',(0.,-1.,0.));
#5304=DIRECTION('ref_axis',(1.,0.,0.));
#5305=DIRECTION('',(0.707106781186548,0.707106781186547,8.65956056235494E-17));
#5306=DIRECTION('center_axis',(0.,-1.,0.));
#5307=DIRECTION('ref_axis',(1.,0.,0.));
#5308=DIRECTION('center_axis',(0.,-1.,0.));
#5309=DIRECTION('ref_axis',(1.,0.,0.));
#5310=DIRECTION('',(0.,1.,0.));
#5311=DIRECTION('center_axis',(0.,1.,0.));
#5312=DIRECTION('ref_axis',(1.,0.,0.));
#5313=DIRECTION('center_axis',(0.,-1.,0.));
#5314=DIRECTION('ref_axis',(1.,0.,0.));
#5315=DIRECTION('',(-0.707106781186547,0.707106781186548,-8.65956056235493E-17));
#5316=DIRECTION('center_axis',(0.,-1.,0.));
#5317=DIRECTION('ref_axis',(0.,0.,-1.));
#5318=DIRECTION('center_axis',(0.,-1.,0.));
#5319=DIRECTION('ref_axis',(1.,0.,0.));
#5320=DIRECTION('center_axis',(0.,1.,0.));
#5321=DIRECTION('ref_axis',(1.,0.,0.));
#5322=DIRECTION('center_axis',(0.,1.,0.));
#5323=DIRECTION('ref_axis',(1.,0.,0.));
#5324=DIRECTION('',(-0.447213595499958,0.894427190999916,-5.47678698264203E-17));
#5325=DIRECTION('center_axis',(0.,-1.,0.));
#5326=DIRECTION('ref_axis',(1.,0.,0.));
#5327=DIRECTION('center_axis',(0.,1.,0.));
#5328=DIRECTION('ref_axis',(1.,0.,0.));
#5329=DIRECTION('',(0.,1.,0.));
#5330=DIRECTION('center_axis',(0.,1.,0.));
#5331=DIRECTION('ref_axis',(1.,0.,0.));
#5332=DIRECTION('center_axis',(0.,-1.,0.));
#5333=DIRECTION('ref_axis',(1.,0.,0.));
#5334=DIRECTION('',(-0.707106781186547,0.707106781186548,-8.65956056235493E-17));
#5335=DIRECTION('center_axis',(0.,-1.,0.));
#5336=DIRECTION('ref_axis',(0.,0.,-1.));
#5337=DIRECTION('center_axis',(0.866025403784439,0.,-0.5));
#5338=DIRECTION('ref_axis',(0.5,0.,0.866025403784439));
#5339=DIRECTION('',(-0.5,0.,-0.866025403784439));
#5340=DIRECTION('',(0.,-1.,0.));
#5341=DIRECTION('',(0.5,0.,0.866025403784439));
#5342=DIRECTION('',(0.,-1.,0.));
#5343=DIRECTION('center_axis',(1.92296268638356E-16,0.,-1.));
#5344=DIRECTION('ref_axis',(1.,0.,1.92296268638356E-16));
#5345=DIRECTION('',(-1.,0.,-1.92296268638356E-16));
#5346=DIRECTION('',(0.,-1.,0.));
#5347=DIRECTION('',(1.,0.,1.92296268638356E-16));
#5348=DIRECTION('center_axis',(-0.866025403784439,0.,-0.5));
#5349=DIRECTION('ref_axis',(0.5,0.,-0.866025403784439));
#5350=DIRECTION('',(-0.5,0.,0.866025403784438));
#5351=DIRECTION('',(0.,-1.,0.));
#5352=DIRECTION('',(0.5,0.,-0.866025403784438));
#5353=DIRECTION('center_axis',(-0.866025403784439,0.,0.5));
#5354=DIRECTION('ref_axis',(-0.5,0.,-0.866025403784439));
#5355=DIRECTION('',(0.5,0.,0.866025403784439));
#5356=DIRECTION('',(0.,-1.,0.));
#5357=DIRECTION('',(-0.5,0.,-0.866025403784439));
#5358=DIRECTION('center_axis',(-1.92296268638356E-16,0.,1.));
#5359=DIRECTION('ref_axis',(-1.,0.,-1.92296268638356E-16));
#5360=DIRECTION('',(1.,0.,1.92296268638356E-16));
#5361=DIRECTION('',(0.,-1.,0.));
#5362=DIRECTION('',(-1.,0.,-1.92296268638356E-16));
#5363=DIRECTION('center_axis',(0.866025403784439,0.,0.5));
#5364=DIRECTION('ref_axis',(-0.5,0.,0.866025403784439));
#5365=DIRECTION('',(0.5,0.,-0.866025403784439));
#5366=DIRECTION('',(-0.5,0.,0.866025403784439));
#5367=DIRECTION('center_axis',(0.,1.,0.));
#5368=DIRECTION('ref_axis',(1.,0.,0.));
#5369=DIRECTION('center_axis',(0.,-1.,0.));
#5370=DIRECTION('ref_axis',(0.,0.,-1.));
#6329=CARTESIAN_POINT('',(0.,0.,0.));
#6330=CARTESIAN_POINT('Origin',(0.45,0.6,0.));
#6331=CARTESIAN_POINT('',(-0.45,0.6,-5.51091059616309E-17));
#6332=CARTESIAN_POINT('Origin',(0.,0.6,0.));
#6333=CARTESIAN_POINT('Origin',(0.,0.575,0.));
#6334=CARTESIAN_POINT('',(-0.5,0.55,-6.12323399573677E-17));
#6335=CARTESIAN_POINT('Origin',(0.,0.55,0.));
#6336=CARTESIAN_POINT('',(-0.475,0.575,-5.81707229594993E-17));
#6337=CARTESIAN_POINT('Origin',(0.,0.29,0.));
#6338=CARTESIAN_POINT('',(-0.5,0.0299999999999998,-6.12323399573677E-17));
#6339=CARTESIAN_POINT('Origin',(0.,0.0299999999999998,0.));
#6340=CARTESIAN_POINT('',(-0.5,0.29,-6.12323399573677E-17));
#6341=CARTESIAN_POINT('Origin',(0.,0.0150000000000001,0.));
#6342=CARTESIAN_POINT('',(-0.47,7.11236625150491E-17,-5.75583995599256E-17));
#6343=CARTESIAN_POINT('Origin',(0.,0.,0.));
#6344=CARTESIAN_POINT('',(-0.485,0.0150000000000001,-5.93953697586466E-17));
#6345=CARTESIAN_POINT('Origin',(0.32,0.,0.));
#6346=CARTESIAN_POINT('',(-0.32,-6.93889390390723E-18,-3.91886975727153E-17));
#6347=CARTESIAN_POINT('Origin',(0.,0.,0.));
#6348=CARTESIAN_POINT('Origin',(0.,-0.02,0.));
#6349=CARTESIAN_POINT('',(-0.2942,-0.0515999999999999,3.60291088309151E-17));
#6350=CARTESIAN_POINT('Origin',(0.,-0.0515999999999999,0.));
#6351=CARTESIAN_POINT('',(-0.31,-0.02,-3.7964050773568E-17));
#6352=CARTESIAN_POINT('Origin',(0.,-1.24,0.));
#6353=CARTESIAN_POINT('',(-0.2942,-2.4458,3.60291088309151E-17));
#6354=CARTESIAN_POINT('Origin',(0.,-2.4458,0.));
#6355=CARTESIAN_POINT('',(-0.2942,-1.24,-3.60291088309151E-17));
#6356=CARTESIAN_POINT('Origin',(0.,-2.47,0.));
#6357=CARTESIAN_POINT('',(-0.24,-2.5,-2.93915231795365E-17));
#6358=CARTESIAN_POINT('Origin',(0.,-2.5,0.));
#6359=CARTESIAN_POINT('',(-0.27,-2.47,-3.30654635769785E-17));
#6360=CARTESIAN_POINT('Origin',(0.,-2.5,0.));
#6361=CARTESIAN_POINT('Origin',(0.144337567297406,-0.6,-0.25));
#6362=CARTESIAN_POINT('',(0.288675134594813,-0.6,0.));
#6363=CARTESIAN_POINT('',(0.144337567297406,-0.6,-0.25));
#6364=CARTESIAN_POINT('',(0.288675134594813,-0.6,0.));
#6365=CARTESIAN_POINT('',(0.144337567297406,-0.96,-0.25));
#6366=CARTESIAN_POINT('',(0.144337567297406,-0.6,-0.25));
#6367=CARTESIAN_POINT('',(0.288675134594813,-0.96,0.));
#6368=CARTESIAN_POINT('',(0.288675134594813,-0.96,0.));
#6369=CARTESIAN_POINT('',(0.288675134594813,-0.6,0.));
#6370=CARTESIAN_POINT('Origin',(-0.144337567297406,-0.6,-0.25));
#6371=CARTESIAN_POINT('',(-0.144337567297406,-0.6,-0.25));
#6372=CARTESIAN_POINT('',(0.144337567297406,-0.6,-0.25));
#6373=CARTESIAN_POINT('',(-0.144337567297406,-0.96,-0.25));
#6374=CARTESIAN_POINT('',(-0.144337567297406,-0.6,-0.25));
#6375=CARTESIAN_POINT('',(0.144337567297406,-0.96,-0.25));
#6376=CARTESIAN_POINT('Origin',(-0.288675134594813,-0.6,-8.32667268468867E-17));
#6377=CARTESIAN_POINT('',(-0.288675134594813,-0.6,-3.53525079574969E-17));
#6378=CARTESIAN_POINT('',(-0.144337567297406,-0.6,-0.25));
#6379=CARTESIAN_POINT('',(-0.288675134594813,-0.96,-5.55111512312578E-17));
#6380=CARTESIAN_POINT('',(-0.288675134594813,-0.6,-3.53525079574969E-17));
#6381=CARTESIAN_POINT('',(-0.144337567297406,-0.96,-0.25));
#6382=CARTESIAN_POINT('Origin',(-0.144337567297407,-0.6,0.25));
#6383=CARTESIAN_POINT('',(-0.144337567297407,-0.6,0.25));
#6384=CARTESIAN_POINT('',(-0.288675134594813,-0.6,-3.53525079574969E-17));
#6385=CARTESIAN_POINT('',(-0.144337567297407,-0.96,0.25));
#6386=CARTESIAN_POINT('',(-0.144337567297407,-0.6,0.25));
#6387=CARTESIAN_POINT('',(-0.288675134594813,-0.96,-3.53525079574969E-17));
#6388=CARTESIAN_POINT('Origin',(0.144337567297406,-0.6,0.25));
#6389=CARTESIAN_POINT('',(0.144337567297406,-0.6,0.25));
#6390=CARTESIAN_POINT('',(-0.144337567297407,-0.6,0.25));
#6391=CARTESIAN_POINT('',(0.144337567297406,-0.96,0.25));
#6392=CARTESIAN_POINT('',(0.144337567297406,-0.6,0.25));
#6393=CARTESIAN_POINT('',(-0.144337567297407,-0.96,0.25));
#6394=CARTESIAN_POINT('Origin',(0.288675134594813,-0.6,0.));
#6395=CARTESIAN_POINT('',(0.144337567297406,-0.6,0.25));
#6396=CARTESIAN_POINT('',(0.144337567297406,-0.96,0.25));
#6397=CARTESIAN_POINT('Origin',(0.,-0.6,0.));
#6398=CARTESIAN_POINT('Origin',(0.,-0.96,0.));
#6441=UNCERTAINTY_MEASURE_WITH_UNIT(LENGTH_MEASURE(0.001),#6464,
'DISTANCE_ACCURACY_VALUE',
'Maximum model space distance between geometric entities at asserted c
onnectivities');
#6442=UNCERTAINTY_MEASURE_WITH_UNIT(LENGTH_MEASURE(0.001),#6464,
'DISTANCE_ACCURACY_VALUE',
'Maximum model space distance between geometric entities at asserted c
onnectivities');
#6462=(
GEOMETRIC_REPRESENTATION_CONTEXT(3)
GLOBAL_UNCERTAINTY_ASSIGNED_CONTEXT((#6441))
GLOBAL_UNIT_ASSIGNED_CONTEXT((#6464,#6466,#6467))
REPRESENTATION_CONTEXT('','3D')
);
#6463=(
GEOMETRIC_REPRESENTATION_CONTEXT(3)
GLOBAL_UNCERTAINTY_ASSIGNED_CONTEXT((#6442))
GLOBAL_UNIT_ASSIGNED_CONTEXT((#6464,#6466,#6467))
REPRESENTATION_CONTEXT('','3D')
);
#6464=(
LENGTH_UNIT()
NAMED_UNIT(*)
SI_UNIT(.CENTI.,.METRE.)
);
#6466=(
NAMED_UNIT(*)
PLANE_ANGLE_UNIT()
SI_UNIT($,.RADIAN.)
);
#6467=(
NAMED_UNIT(*)
SI_UNIT($,.STERADIAN.)
SOLID_ANGLE_UNIT()
);
#6487=SHAPE_DEFINITION_REPRESENTATION(#6536,#6579);
#6536=PRODUCT_DEFINITION_SHAPE('',$,#6600);
#6579=SHAPE_REPRESENTATION('',(#4218),#6462);
#6580=PRODUCT_DEFINITION_CONTEXT('part definition',#6642,'design');
#6600=PRODUCT_DEFINITION('Cap Screw - M6x25','Cap Screw - M6x25',#6620,
#6580);
#6620=PRODUCT_DEFINITION_FORMATION('',$,#6663);
#6642=APPLICATION_CONTEXT(
'Core Data for Automotive Mechanical Design Process');
#6643=PRODUCT_CONTEXT('part definition',#6642,'mechanical');
#6663=PRODUCT('Cap Screw - M6x25','Cap Screw - M6x25',
'Cap Screw - M6x25',(#6643));
#6741=COLOUR_RGB('Black',0.12,0.14,0.17);
#6742=FILL_AREA_STYLE_COLOUR('',#6741);
#6743=FILL_AREA_STYLE('',(#6742));
#6744=SURFACE_STYLE_FILL_AREA(#6743);
#6745=SURFACE_SIDE_STYLE('',(#6744));
#6746=SURFACE_STYLE_USAGE(.BOTH.,#6745);
#6747=PRESENTATION_STYLE_ASSIGNMENT((#6746));
ENDSEC;
END-ISO-10303-21;
